ISO-10303-21;
HEADER;
/* Generated by software containing ST-Developer
 * from STEP Tools, Inc. (www.steptools.com) 
 */

FILE_DESCRIPTION(
/* description */ ('Hinged panel with latch'),
/* implementation_level */ '2;1');

FILE_NAME(
/* name */ 'Slot Nut - M5 for 20 mm Extrusion.step',
/* time_stamp */ '2026-10-27T20:36:01-07:00',
/* author */ (''),
/* organization */ (''),
/* preprocessor_version */ 'ST-DEVELOPER v20.2',
/* originating_system */ 'Autodesk Translation Framework v15.17.0.0',
/* authorisation */ '');

FILE_SCHEMA (('AUTOMOTIVE_DESIGN { 1 0 10303 214 3 1 1 }'));
ENDSEC;

DATA;
#10=MECHANICAL_DESIGN_GEOMETRIC_PRESENTATION_REPRESENTATION('',(#302),#6743);
#237=ELLIPSE('',#4125,0.299389011154384,0.2117);
#238=ELLIPSE('',#4130,0.299389011154384,0.2117);
#270=SHAPE_REPRESENTATION_RELATIONSHIP('SRR','None',#6845,#286);
#286=ADVANCED_BREP_SHAPE_REPRESENTATION('',(#318),#6731);
#302=STYLED_ITEM('',(#7010),#318);
#318=MANIFOLD_SOLID_BREP('Body1',#3804);
#344=FACE_BOUND('',#846,.T.);
#442=PLANE('',#4124);
#443=PLANE('',#4132);
#444=PLANE('',#4133);
#445=PLANE('',#4134);
#446=PLANE('',#4135);
#447=PLANE('',#4136);
#448=PLANE('',#4137);
#449=PLANE('',#4138);
#450=PLANE('',#4139);
#611=FACE_OUTER_BOUND('',#836,.T.);
#612=FACE_OUTER_BOUND('',#837,.T.);
#613=FACE_OUTER_BOUND('',#838,.T.);
#614=FACE_OUTER_BOUND('',#839,.T.);
#615=FACE_OUTER_BOUND('',#840,.T.);
#616=FACE_OUTER_BOUND('',#841,.T.);
#617=FACE_OUTER_BOUND('',#842,.T.);
#618=FACE_OUTER_BOUND('',#843,.T.);
#619=FACE_OUTER_BOUND('',#844,.T.);
#620=FACE_OUTER_BOUND('',#845,.T.);
#836=EDGE_LOOP('',(#3048,#3049,#3050,#3051,#3052,#3053));
#837=EDGE_LOOP('',(#3054,#3055,#3056,#3057,#3058,#3059,#3060,#3061));
#838=EDGE_LOOP('',(#3062,#3063,#3064,#3065,#3066));
#839=EDGE_LOOP('',(#3067,#3068,#3069,#3070));
#840=EDGE_LOOP('',(#3071,#3072,#3073,#3074,#3075,#3076));
#841=EDGE_LOOP('',(#3077,#3078,#3079,#3080,#3081,#3082));
#842=EDGE_LOOP('',(#3083,#3084,#3085,#3086));
#843=EDGE_LOOP('',(#3087,#3088,#3089,#3090));
#844=EDGE_LOOP('',(#3091,#3092,#3093,#3094,#3095,#3096));
#845=EDGE_LOOP('',(#3097,#3098,#3099,#3100));
#846=EDGE_LOOP('',(#3101));
#1172=LINE('',#6061,#1530);
#1173=LINE('',#6063,#1531);
#1174=LINE('',#6065,#1532);
#1175=LINE('',#6067,#1533);
#1176=LINE('',#6070,#1534);
#1177=LINE('',#6075,#1535);
#1178=LINE('',#6084,#1536);
#1179=LINE('',#6085,#1537);
#1180=LINE('',#6088,#1538);
#1181=LINE('',#6089,#1539);
#1182=LINE('',#6092,#1540);
#1183=LINE('',#6094,#1541);
#1184=LINE('',#6095,#1542);
#1185=LINE('',#6098,#1543);
#1186=LINE('',#6100,#1544);
#1187=LINE('',#6101,#1545);
#1188=LINE('',#6104,#1546);
#1189=LINE('',#6105,#1547);
#1190=LINE('',#6108,#1548);
#1191=LINE('',#6109,#1549);
#1192=LINE('',#6111,#1550);
#1530=VECTOR('',#4816,1.);
#1531=VECTOR('',#4817,1.);
#1532=VECTOR('',#4818,1.);
#1533=VECTOR('',#4819,1.);
#1534=VECTOR('',#4822,1.);
#1535=VECTOR('',#4827,0.21);
#1536=VECTOR('',#4838,1.);
#1537=VECTOR('',#4839,1.);
#1538=VECTOR('',#4842,1.);
#1539=VECTOR('',#4843,1.);
#1540=VECTOR('',#4846,1.);
#1541=VECTOR('',#4847,1.);
#1542=VECTOR('',#4848,1.);
#1543=VECTOR('',#4851,1.);
#1544=VECTOR('',#4852,1.);
#1545=VECTOR('',#4853,1.);
#1546=VECTOR('',#4856,1.);
#1547=VECTOR('',#4857,1.);
#1548=VECTOR('',#4860,1.);
#1549=VECTOR('',#4861,1.);
#1550=VECTOR('',#4864,1.);
#1731=CIRCLE('',#4127,0.2117);
#1732=CIRCLE('',#4128,0.2117);
#1733=CIRCLE('',#4129,0.2117);
#1734=CIRCLE('',#4131,0.2117);
#1943=VERTEX_POINT('',#6059);
#1944=VERTEX_POINT('',#6060);
#1945=VERTEX_POINT('',#6062);
#1946=VERTEX_POINT('',#6064);
#1947=VERTEX_POINT('',#6066);
#1948=VERTEX_POINT('',#6068);
#1949=VERTEX_POINT('',#6072);
#1950=VERTEX_POINT('',#6074);
#1951=VERTEX_POINT('',#6077);
#1952=VERTEX_POINT('',#6079);
#1953=VERTEX_POINT('',#6083);
#1954=VERTEX_POINT('',#6087);
#1955=VERTEX_POINT('',#6091);
#1956=VERTEX_POINT('',#6093);
#1957=VERTEX_POINT('',#6097);
#1958=VERTEX_POINT('',#6099);
#1959=VERTEX_POINT('',#6103);
#1960=VERTEX_POINT('',#6107);
#2336=EDGE_CURVE('',#1943,#1944,#1172,.T.);
#2337=EDGE_CURVE('',#1944,#1945,#1173,.T.);
#2338=EDGE_CURVE('',#1945,#1946,#1174,.T.);
#2339=EDGE_CURVE('',#1946,#1947,#1175,.T.);
#2340=EDGE_CURVE('',#1947,#1948,#237,.T.);
#2341=EDGE_CURVE('',#1948,#1943,#1176,.T.);
#2342=EDGE_CURVE('',#1949,#1947,#1731,.F.);
#2343=EDGE_CURVE('',#1949,#1950,#1177,.T.);
#2344=EDGE_CURVE('',#1950,#1950,#1732,.T.);
#2345=EDGE_CURVE('',#1951,#1949,#1733,.F.);
#2346=EDGE_CURVE('',#1952,#1951,#238,.T.);
#2347=EDGE_CURVE('',#1948,#1952,#1734,.F.);
#2348=EDGE_CURVE('',#1953,#1946,#1178,.T.);
#2349=EDGE_CURVE('',#1951,#1953,#1179,.T.);
#2350=EDGE_CURVE('',#1954,#1952,#1180,.T.);
#2351=EDGE_CURVE('',#1943,#1954,#1181,.T.);
#2352=EDGE_CURVE('',#1953,#1955,#1182,.T.);
#2353=EDGE_CURVE('',#1955,#1956,#1183,.T.);
#2354=EDGE_CURVE('',#1956,#1954,#1184,.T.);
#2355=EDGE_CURVE('',#1956,#1957,#1185,.T.);
#2356=EDGE_CURVE('',#1958,#1957,#1186,.T.);
#2357=EDGE_CURVE('',#1944,#1958,#1187,.T.);
#2358=EDGE_CURVE('',#1955,#1959,#1188,.T.);
#2359=EDGE_CURVE('',#1957,#1959,#1189,.T.);
#2360=EDGE_CURVE('',#1960,#1958,#1190,.T.);
#2361=EDGE_CURVE('',#1945,#1960,#1191,.T.);
#2362=EDGE_CURVE('',#1959,#1960,#1192,.T.);
#3048=ORIENTED_EDGE('',*,*,#2336,.T.);
#3049=ORIENTED_EDGE('',*,*,#2337,.T.);
#3050=ORIENTED_EDGE('',*,*,#2338,.T.);
#3051=ORIENTED_EDGE('',*,*,#2339,.T.);
#3052=ORIENTED_EDGE('',*,*,#2340,.T.);
#3053=ORIENTED_EDGE('',*,*,#2341,.T.);
#3054=ORIENTED_EDGE('',*,*,#2340,.F.);
#3055=ORIENTED_EDGE('',*,*,#2342,.F.);
#3056=ORIENTED_EDGE('',*,*,#2343,.T.);
#3057=ORIENTED_EDGE('',*,*,#2344,.F.);
#3058=ORIENTED_EDGE('',*,*,#2343,.F.);
#3059=ORIENTED_EDGE('',*,*,#2345,.F.);
#3060=ORIENTED_EDGE('',*,*,#2346,.F.);
#3061=ORIENTED_EDGE('',*,*,#2347,.F.);
#3062=ORIENTED_EDGE('',*,*,#2339,.F.);
#3063=ORIENTED_EDGE('',*,*,#2348,.F.);
#3064=ORIENTED_EDGE('',*,*,#2349,.F.);
#3065=ORIENTED_EDGE('',*,*,#2345,.T.);
#3066=ORIENTED_EDGE('',*,*,#2342,.T.);
#3067=ORIENTED_EDGE('',*,*,#2341,.F.);
#3068=ORIENTED_EDGE('',*,*,#2347,.T.);
#3069=ORIENTED_EDGE('',*,*,#2350,.F.);
#3070=ORIENTED_EDGE('',*,*,#2351,.F.);
#3071=ORIENTED_EDGE('',*,*,#2352,.T.);
#3072=ORIENTED_EDGE('',*,*,#2353,.T.);
#3073=ORIENTED_EDGE('',*,*,#2354,.T.);
#3074=ORIENTED_EDGE('',*,*,#2350,.T.);
#3075=ORIENTED_EDGE('',*,*,#2346,.T.);
#3076=ORIENTED_EDGE('',*,*,#2349,.T.);
#3077=ORIENTED_EDGE('',*,*,#2336,.F.);
#3078=ORIENTED_EDGE('',*,*,#2351,.T.);
#3079=ORIENTED_EDGE('',*,*,#2354,.F.);
#3080=ORIENTED_EDGE('',*,*,#2355,.T.);
#3081=ORIENTED_EDGE('',*,*,#2356,.F.);
#3082=ORIENTED_EDGE('',*,*,#2357,.F.);
#3083=ORIENTED_EDGE('',*,*,#2353,.F.);
#3084=ORIENTED_EDGE('',*,*,#2358,.T.);
#3085=ORIENTED_EDGE('',*,*,#2359,.F.);
#3086=ORIENTED_EDGE('',*,*,#2355,.F.);
#3087=ORIENTED_EDGE('',*,*,#2337,.F.);
#3088=ORIENTED_EDGE('',*,*,#2357,.T.);
#3089=ORIENTED_EDGE('',*,*,#2360,.F.);
#3090=ORIENTED_EDGE('',*,*,#2361,.F.);
#3091=ORIENTED_EDGE('',*,*,#2338,.F.);
#3092=ORIENTED_EDGE('',*,*,#2361,.T.);
#3093=ORIENTED_EDGE('',*,*,#2362,.F.);
#3094=ORIENTED_EDGE('',*,*,#2358,.F.);
#3095=ORIENTED_EDGE('',*,*,#2352,.F.);
#3096=ORIENTED_EDGE('',*,*,#2348,.T.);
#3097=ORIENTED_EDGE('',*,*,#2362,.T.);
#3098=ORIENTED_EDGE('',*,*,#2360,.T.);
#3099=ORIENTED_EDGE('',*,*,#2356,.T.);
#3100=ORIENTED_EDGE('',*,*,#2359,.T.);
#3101=ORIENTED_EDGE('',*,*,#2344,.T.);
#3571=CYLINDRICAL_SURFACE('',#4126,0.2117);
#3680=ADVANCED_FACE('',(#611),#442,.T.);
#3681=ADVANCED_FACE('',(#612),#3571,.F.);
#3682=ADVANCED_FACE('',(#613),#443,.F.);
#3683=ADVANCED_FACE('',(#614),#444,.F.);
#3684=ADVANCED_FACE('',(#615),#445,.T.);
#3685=ADVANCED_FACE('',(#616),#446,.T.);
#3686=ADVANCED_FACE('',(#617),#447,.T.);
#3687=ADVANCED_FACE('',(#618),#448,.T.);
#3688=ADVANCED_FACE('',(#619),#449,.T.);
#3689=ADVANCED_FACE('',(#620,#344),#450,.T.);
#3804=CLOSED_SHELL('',(#3680,#3681,#3682,#3683,#3684,#3685,#3686,#3687,
#3688,#3689));
#4123=AXIS2_PLACEMENT_3D('',#6057,#4812,#4813);
#4124=AXIS2_PLACEMENT_3D('',#6058,#4814,#4815);
#4125=AXIS2_PLACEMENT_3D('',#6069,#4820,#4821);
#4126=AXIS2_PLACEMENT_3D('',#6071,#4823,#4824);
#4127=AXIS2_PLACEMENT_3D('',#6073,#4825,#4826);
#4128=AXIS2_PLACEMENT_3D('',#6076,#4828,#4829);
#4129=AXIS2_PLACEMENT_3D('',#6078,#4830,#4831);
#4130=AXIS2_PLACEMENT_3D('',#6080,#4832,#4833);
#4131=AXIS2_PLACEMENT_3D('',#6081,#4834,#4835);
#4132=AXIS2_PLACEMENT_3D('',#6082,#4836,#4837);
#4133=AXIS2_PLACEMENT_3D('',#6086,#4840,#4841);
#4134=AXIS2_PLACEMENT_3D('',#6090,#4844,#4845);
#4135=AXIS2_PLACEMENT_3D('',#6096,#4849,#4850);
#4136=AXIS2_PLACEMENT_3D('',#6102,#4854,#4855);
#4137=AXIS2_PLACEMENT_3D('',#6106,#4858,#4859);
#4138=AXIS2_PLACEMENT_3D('',#6110,#4862,#4863);
#4139=AXIS2_PLACEMENT_3D('',#6112,#4865,#4866);
#4812=DIRECTION('axis',(0.,0.,1.));
#4813=DIRECTION('refdir',(1.,0.,0.));
#4814=DIRECTION('center_axis',(0.,-0.707106781186548,-0.707106781186548));
#4815=DIRECTION('ref_axis',(-1.,0.,0.));
#4816=DIRECTION('',(0.,-0.707106781186548,0.707106781186548));
#4817=DIRECTION('',(-1.,0.,0.));
#4818=DIRECTION('',(0.,0.707106781186548,-0.707106781186548));
#4819=DIRECTION('',(1.,0.,0.));
#4820=DIRECTION('center_axis',(0.,0.707106781186548,0.707106781186548));
#4821=DIRECTION('ref_axis',(0.,0.707106781186547,-0.707106781186547));
#4822=DIRECTION('',(1.,0.,0.));
#4823=DIRECTION('center_axis',(0.,0.,1.));
#4824=DIRECTION('ref_axis',(1.,0.,0.));
#4825=DIRECTION('center_axis',(0.,0.,-1.));
#4826=DIRECTION('ref_axis',(1.,0.,0.));
#4827=DIRECTION('',(0.,0.,1.));
#4828=DIRECTION('center_axis',(0.,0.,-1.));
#4829=DIRECTION('ref_axis',(1.,0.,0.));
#4830=DIRECTION('center_axis',(0.,0.,-1.));
#4831=DIRECTION('ref_axis',(1.,0.,0.));
#4832=DIRECTION('center_axis',(0.,-0.707106781186548,0.707106781186548));
#4833=DIRECTION('ref_axis',(0.,0.707106781186547,0.707106781186547));
#4834=DIRECTION('center_axis',(0.,0.,-1.));
#4835=DIRECTION('ref_axis',(1.,0.,0.));
#4836=DIRECTION('center_axis',(0.,0.,1.));
#4837=DIRECTION('ref_axis',(1.,0.,0.));
#4838=DIRECTION('',(0.,-1.,0.));
#4839=DIRECTION('',(-1.,0.,0.));
#4840=DIRECTION('center_axis',(0.,0.,1.));
#4841=DIRECTION('ref_axis',(1.,0.,0.));
#4842=DIRECTION('',(-1.,0.,0.));
#4843=DIRECTION('',(0.,1.,0.));
#4844=DIRECTION('center_axis',(0.,0.707106781186548,-0.707106781186548));
#4845=DIRECTION('ref_axis',(-1.,0.,0.));
#4846=DIRECTION('',(0.,0.707106781186548,0.707106781186548));
#4847=DIRECTION('',(1.,0.,0.));
#4848=DIRECTION('',(0.,-0.707106781186548,-0.707106781186548));
#4849=DIRECTION('center_axis',(1.,0.,0.));
#4850=DIRECTION('ref_axis',(0.,1.,0.));
#4851=DIRECTION('',(0.,0.,1.));
#4852=DIRECTION('',(0.,1.,0.));
#4853=DIRECTION('',(0.,0.,1.));
#4854=DIRECTION('center_axis',(0.,1.,0.));
#4855=DIRECTION('ref_axis',(-1.,0.,0.));
#4856=DIRECTION('',(0.,0.,1.));
#4857=DIRECTION('',(-1.,0.,0.));
#4858=DIRECTION('center_axis',(0.,-1.,0.));
#4859=DIRECTION('ref_axis',(1.,0.,0.));
#4860=DIRECTION('',(1.,0.,0.));
#4861=DIRECTION('',(0.,0.,1.));
#4862=DIRECTION('center_axis',(-1.,0.,0.));
#4863=DIRECTION('ref_axis',(0.,-1.,0.));
#4864=DIRECTION('',(0.,-1.,0.));
#4865=DIRECTION('center_axis',(0.,0.,1.));
#4866=DIRECTION('ref_axis',(1.,0.,0.));
#6057=CARTESIAN_POINT('',(0.,0.,0.));
#6058=CARTESIAN_POINT('Origin',(-0.25,-0.225,0.075));
#6059=CARTESIAN_POINT('',(0.5,-0.15,0.));
#6060=CARTESIAN_POINT('',(0.5,-0.3,0.15));
#6061=CARTESIAN_POINT('',(0.5,-0.225,0.075));
#6062=CARTESIAN_POINT('',(-0.5,-0.3,0.15));
#6063=CARTESIAN_POINT('',(-0.25,-0.3,0.15));
#6064=CARTESIAN_POINT('',(-0.5,-0.15,0.));
#6065=CARTESIAN_POINT('',(-0.5,-0.075,-0.075));
#6066=CARTESIAN_POINT('',(-0.149388386429468,-0.15,0.));
#6067=CARTESIAN_POINT('',(-0.25,-0.15,0.));
#6068=CARTESIAN_POINT('',(0.149388386429468,-0.15,0.));
#6069=CARTESIAN_POINT('Origin',(0.,0.,-0.15));
#6070=CARTESIAN_POINT('',(-0.25,-0.15,0.));
#6071=CARTESIAN_POINT('Origin',(0.,0.,-0.1));
#6072=CARTESIAN_POINT('',(-0.2117,-2.59257727379495E-17,0.));
#6073=CARTESIAN_POINT('Origin',(0.,0.,0.));
#6074=CARTESIAN_POINT('',(-0.2117,2.59257727379495E-17,0.4));
#6075=CARTESIAN_POINT('',(-0.2117,-2.59257727379495E-17,-0.1));
#6076=CARTESIAN_POINT('Origin',(0.,0.,0.4));
#6077=CARTESIAN_POINT('',(-0.149388386429468,0.15,0.));
#6078=CARTESIAN_POINT('Origin',(0.,0.,0.));
#6079=CARTESIAN_POINT('',(0.149388386429468,0.15,0.));
#6080=CARTESIAN_POINT('Origin',(0.,0.,-0.15));
#6081=CARTESIAN_POINT('Origin',(0.,0.,0.));
#6082=CARTESIAN_POINT('Origin',(0.,0.,0.));
#6083=CARTESIAN_POINT('',(-0.5,0.15,0.));
#6084=CARTESIAN_POINT('',(-0.5,0.3,0.));
#6085=CARTESIAN_POINT('',(0.25,0.15,0.));
#6086=CARTESIAN_POINT('Origin',(0.,0.,0.));
#6087=CARTESIAN_POINT('',(0.5,0.15,0.));
#6088=CARTESIAN_POINT('',(0.25,0.15,0.));
#6089=CARTESIAN_POINT('',(0.5,-0.3,0.));
#6090=CARTESIAN_POINT('Origin',(0.25,0.225,0.075));
#6091=CARTESIAN_POINT('',(-0.5,0.3,0.15));
#6092=CARTESIAN_POINT('',(-0.5,0.225,0.075));
#6093=CARTESIAN_POINT('',(0.5,0.3,0.15));
#6094=CARTESIAN_POINT('',(0.25,0.3,0.15));
#6095=CARTESIAN_POINT('',(0.5,0.075,-0.075));
#6096=CARTESIAN_POINT('Origin',(0.5,-0.3,0.));
#6097=CARTESIAN_POINT('',(0.5,0.3,0.4));
#6098=CARTESIAN_POINT('',(0.5,0.3,0.));
#6099=CARTESIAN_POINT('',(0.5,-0.3,0.4));
#6100=CARTESIAN_POINT('',(0.5,-0.3,0.4));
#6101=CARTESIAN_POINT('',(0.5,-0.3,0.));
#6102=CARTESIAN_POINT('Origin',(0.5,0.3,0.));
#6103=CARTESIAN_POINT('',(-0.5,0.3,0.4));
#6104=CARTESIAN_POINT('',(-0.5,0.3,0.));
#6105=CARTESIAN_POINT('',(0.5,0.3,0.4));
#6106=CARTESIAN_POINT('Origin',(-0.5,-0.3,0.));
#6107=CARTESIAN_POINT('',(-0.5,-0.3,0.4));
#6108=CARTESIAN_POINT('',(-0.5,-0.3,0.4));
#6109=CARTESIAN_POINT('',(-0.5,-0.3,0.));
#6110=CARTESIAN_POINT('Origin',(-0.5,0.3,0.));
#6111=CARTESIAN_POINT('',(-0.5,0.3,0.4));
#6112=CARTESIAN_POINT('Origin',(0.,0.,0.4));
#6710=UNCERTAINTY_MEASURE_WITH_UNIT(LENGTH_MEASURE(0.001),#6744,
'DISTANCE_ACCURACY_VALUE',
'Maximum model space distance between geometric entities at asserted c
onnectivities');
#6722=UNCERTAINTY_MEASURE_WITH_UNIT(LENGTH_MEASURE(0.001),#6744,
'DISTANCE_ACCURACY_VALUE',
'Maximum model space distance between geometric entities at asserted c
onnectivities');
#6731=(
GEOMETRIC_REPRESENTATION_CONTEXT(3)
GLOBAL_UNCERTAINTY_ASSIGNED_CONTEXT((#6710))
GLOBAL_UNIT_ASSIGNED_CONTEXT((#6744,#6746,#6747))
REPRESENTATION_CONTEXT('','3D')
);
#6743=(
GEOMETRIC_REPRESENTATION_CONTEXT(3)
GLOBAL_UNCERTAINTY_ASSIGNED_CONTEXT((#6722))
GLOBAL_UNIT_ASSIGNED_CONTEXT((#6744,#6746,#6747))
REPRESENTATION_CONTEXT('','3D')
);
#6744=(
LENGTH_UNIT()
NAMED_UNIT(*)
SI_UNIT(.CENTI.,.METRE.)
);
#6746=(
NAMED_UNIT(*)
PLANE_ANGLE_UNIT()
SI_UNIT($,.RADIAN.)
);
#6747=(
NAMED_UNIT(*)
SI_UNIT($,.STERADIAN.)
SOLID_ANGLE_UNIT()
);
#6756=SHAPE_DEFINITION_REPRESENTATION(#6776,#6845);
#6776=PRODUCT_DEFINITION_SHAPE('',$,#6866);
#6845=SHAPE_REPRESENTATION('',(#4123),#6731);
#6857=PRODUCT_DEFINITION_CONTEXT('part definition',#6919,'design');
#6866=PRODUCT_DEFINITION('Slot Nut - M5 for 20 mm Extrusion',
'Slot Nut - M5 for 20 mm Extrusion',#6886,#6857);
#6886=PRODUCT_DEFINITION_FORMATION('',$,#6929);
#6919=APPLICATION_CONTEXT(
'Core Data for Automotive Mechanical Design Process');
#6920=PRODUCT_CONTEXT('part definition',#6919,'mechanical');
#6929=PRODUCT('Slot Nut - M5 for 20 mm Extrusion',
'Slot Nut - M5 for 20 mm Extrusion','Slot Nut - M5 for 20 mm Extrusion',
(#6920));
#7004=COLOUR_RGB('Black',0.12,0.14,0.17);
#7005=FILL_AREA_STYLE_COLOUR('',#7004);
#7006=FILL_AREA_STYLE('',(#7005));
#7007=SURFACE_STYLE_FILL_AREA(#7006);
#7008=SURFACE_SIDE_STYLE('',(#7007));
#7009=SURFACE_STYLE_USAGE(.BOTH.,#7008);
#7010=PRESENTATION_STYLE_ASSIGNMENT((#7009));
ENDSEC;
END-ISO-10303-21;
